ISO-10303-21;
HEADER;
/* Generated by software containing ST-Developer
 * from STEP Tools, Inc. (www.steptools.com) 
 */

FILE_DESCRIPTION(
/* description */ ('STEP AP214'),
/* implementation_level */ '2;1');

FILE_NAME(
/* name */ 'PRT-RH-1004-04.step',
/* time_stamp */ '2026-10-07T12:49:37-07:00',
/* author */ (''),
/* organization */ (''),
/* preprocessor_version */ 'ST-DEVELOPER v20.2',
/* originating_system */ 'Autodesk Translation Framework v15.15.0.0',
/* authorisation */ '');

FILE_SCHEMA (('AUTOMOTIVE_DESIGN { 1 0 10303 214 3 1 1 }'));
ENDSEC;

DATA;
#10=MECHANICAL_DESIGN_GEOMETRIC_PRESENTATION_REPRESENTATION('',(#291),#33016);
#237=SHAPE_REPRESENTATION_RELATIONSHIP('SRR','None',#33130,#264);
#264=ADVANCED_BREP_SHAPE_REPRESENTATION('',(#322),#32991);
#291=STYLED_ITEM('',(#33284),#322);
#322=MANIFOLD_SOLID_BREP('Body1',#9946);
#353=CONICAL_SURFACE('',#10660,4.50000000000001,0.785398163397445);
#354=CONICAL_SURFACE('',#10661,14.5,0.785398163397447);
#493=FACE_BOUND('',#1815,.T.);
#494=FACE_BOUND('',#1817,.T.);
#495=FACE_BOUND('',#1820,.T.);
#579=B_SPLINE_CURVE_WITH_KNOTS('',3,(#18006,#18007,#18008,#18009,#18010,
#18011,#18012,#18013,#18014,#18015,#18016,#18017,#18018,#18019,#18020,#18021,
#18022,#18023),.UNSPECIFIED.,.F.,.F.,(4,2,2,2,2,2,2,2,4),(0.866318752317526,
0.974859456130365,1.08340015994321,1.19143914420975,1.29947812847629,1.40751711274283,
1.51555609700937,1.62409680082221,1.73263750463505),.UNSPECIFIED.);
#580=B_SPLINE_CURVE_WITH_KNOTS('',3,(#18024,#18025,#18026,#18027,#18028,
#18029,#18030,#18031,#18032,#18033,#18034,#18035,#18036,#18037,#18038,#18039,
#18040,#18041),.UNSPECIFIED.,.F.,.F.,(4,2,2,2,2,2,2,2,4),(1.73263750463505,
1.84117820844789,1.94971891226073,2.05775789652727,2.16579688079381,2.27383586506035,
2.3818748493269,2.49041555313974,2.59895625695258),.UNSPECIFIED.);
#887=PLANE('',#10627);
#888=PLANE('',#10633);
#889=PLANE('',#10639);
#890=PLANE('',#10648);
#891=PLANE('',#10651);
#892=PLANE('',#10652);
#893=PLANE('',#10659);
#1238=FACE_OUTER_BOUND('',#1813,.T.);
#1239=FACE_OUTER_BOUND('',#1814,.T.);
#1240=FACE_OUTER_BOUND('',#1816,.T.);
#1241=FACE_OUTER_BOUND('',#1818,.T.);
#1242=FACE_OUTER_BOUND('',#1819,.T.);
#1243=FACE_OUTER_BOUND('',#1821,.T.);
#1244=FACE_OUTER_BOUND('',#1822,.T.);
#1245=FACE_OUTER_BOUND('',#1823,.T.);
#1246=FACE_OUTER_BOUND('',#1824,.T.);
#1247=FACE_OUTER_BOUND('',#1825,.T.);
#1248=FACE_OUTER_BOUND('',#1826,.T.);
#1249=FACE_OUTER_BOUND('',#1827,.T.);
#1250=FACE_OUTER_BOUND('',#1828,.T.);
#1251=FACE_OUTER_BOUND('',#1829,.T.);
#1252=FACE_OUTER_BOUND('',#1830,.T.);
#1253=FACE_OUTER_BOUND('',#1831,.T.);
#1254=FACE_OUTER_BOUND('',#1832,.T.);
#1255=FACE_OUTER_BOUND('',#1833,.T.);
#1813=EDGE_LOOP('',(#7586));
#1814=EDGE_LOOP('',(#7587,#7588,#7589,#7590,#7591));
#1815=EDGE_LOOP('',(#7592,#7593));
#1816=EDGE_LOOP('',(#7594));
#1817=EDGE_LOOP('',(#7595));
#1818=EDGE_LOOP('',(#7596,#7597,#7598,#7599,#7600));
#1819=EDGE_LOOP('',(#7601));
#1820=EDGE_LOOP('',(#7602,#7603,#7604,#7605,#7606,#7607,#7608,#7609));
#1821=EDGE_LOOP('',(#7610,#7611,#7612,#7613));
#1822=EDGE_LOOP('',(#7614,#7615,#7616,#7617));
#1823=EDGE_LOOP('',(#7618,#7619,#7620,#7621));
#1824=EDGE_LOOP('',(#7622,#7623,#7624,#7625));
#1825=EDGE_LOOP('',(#7626,#7627,#7628,#7629,#7630,#7631,#7632,#7633));
#1826=EDGE_LOOP('',(#7634,#7635,#7636,#7637,#7638));
#1827=EDGE_LOOP('',(#7639));
#1828=EDGE_LOOP('',(#7640,#7641,#7642,#7643,#7644));
#1829=EDGE_LOOP('',(#7645,#7646,#7647,#7648,#7649));
#1830=EDGE_LOOP('',(#7650,#7651,#7652,#7653));
#1831=EDGE_LOOP('',(#7654,#7655,#7656,#7657));
#1832=EDGE_LOOP('',(#7658,#7659,#7660,#7661));
#1833=EDGE_LOOP('',(#7662,#7663,#7664,#7665));
#2358=CIRCLE('',#10628,4.50000000000001);
#2359=CIRCLE('',#10630,5.);
#2360=CIRCLE('',#10631,5.);
#2361=CIRCLE('',#10632,5.);
#2362=CIRCLE('',#10634,14.5);
#2363=CIRCLE('',#10636,15.);
#2364=CIRCLE('',#10637,15.);
#2365=CIRCLE('',#10638,15.);
#2366=CIRCLE('',#10640,12.5);
#2367=CIRCLE('',#10641,1.);
#2368=CIRCLE('',#10642,1.);
#2369=CIRCLE('',#10643,12.5);
#2370=CIRCLE('',#10644,1.);
#2371=CIRCLE('',#10645,1.);
#2372=CIRCLE('',#10647,12.5);
#2373=CIRCLE('',#10650,12.5);
#2374=CIRCLE('',#10653,1.);
#2375=CIRCLE('',#10654,1.);
#2376=CIRCLE('',#10655,1.);
#2377=CIRCLE('',#10656,1.);
#2378=CIRCLE('',#10658,2.8);
#2997=LINE('',#18001,#3747);
#2998=LINE('',#18050,#3748);
#2999=LINE('',#18060,#3749);
#3000=LINE('',#18068,#3750);
#3001=LINE('',#18074,#3751);
#3002=LINE('',#18075,#3752);
#3003=LINE('',#18078,#3753);
#3004=LINE('',#18080,#3754);
#3005=LINE('',#18081,#3755);
#3006=LINE('',#18084,#3756);
#3007=LINE('',#18087,#3757);
#3008=LINE('',#18090,#3758);
#3009=LINE('',#18092,#3759);
#3010=LINE('',#18093,#3760);
#3011=LINE('',#18102,#3761);
#3012=LINE('',#18105,#3762);
#3013=LINE('',#18107,#3763);
#3747=VECTOR('',#12358,5.);
#3748=VECTOR('',#12371,15.);
#3749=VECTOR('',#12382,1000.);
#3750=VECTOR('',#12389,1000.);
#3751=VECTOR('',#12396,1000.);
#3752=VECTOR('',#12397,1000.);
#3753=VECTOR('',#12400,1000.);
#3754=VECTOR('',#12401,1000.);
#3755=VECTOR('',#12402,1000.);
#3756=VECTOR('',#12405,1000.);
#3757=VECTOR('',#12408,1000.);
#3758=VECTOR('',#12411,1000.);
#3759=VECTOR('',#12412,1000.);
#3760=VECTOR('',#12413,1000.);
#3761=VECTOR('',#12428,2.8);
#3762=VECTOR('',#12433,4.50000000000001);
#3763=VECTOR('',#12436,14.5);
#4480=VERTEX_POINT('',#17994);
#4481=VERTEX_POINT('',#17997);
#4482=VERTEX_POINT('',#17998);
#4483=VERTEX_POINT('',#18000);
#4484=VERTEX_POINT('',#18004);
#4485=VERTEX_POINT('',#18005);
#4486=VERTEX_POINT('',#18043);
#4487=VERTEX_POINT('',#18046);
#4488=VERTEX_POINT('',#18047);
#4489=VERTEX_POINT('',#18049);
#4490=VERTEX_POINT('',#18054);
#4491=VERTEX_POINT('',#18055);
#4492=VERTEX_POINT('',#18057);
#4493=VERTEX_POINT('',#18059);
#4494=VERTEX_POINT('',#18061);
#4495=VERTEX_POINT('',#18063);
#4496=VERTEX_POINT('',#18065);
#4497=VERTEX_POINT('',#18067);
#4498=VERTEX_POINT('',#18071);
#4499=VERTEX_POINT('',#18072);
#4500=VERTEX_POINT('',#18077);
#4501=VERTEX_POINT('',#18079);
#4502=VERTEX_POINT('',#18083);
#4503=VERTEX_POINT('',#18085);
#4504=VERTEX_POINT('',#18089);
#4505=VERTEX_POINT('',#18091);
#4506=VERTEX_POINT('',#18100);
#5606=EDGE_CURVE('',#4480,#4480,#2358,.T.);
#5607=EDGE_CURVE('',#4481,#4482,#2359,.T.);
#5608=EDGE_CURVE('',#4482,#4483,#2997,.T.);
#5609=EDGE_CURVE('',#4483,#4483,#2360,.T.);
#5610=EDGE_CURVE('',#4482,#4481,#2361,.T.);
#5611=EDGE_CURVE('',#4484,#4485,#579,.T.);
#5612=EDGE_CURVE('',#4485,#4484,#580,.T.);
#5613=EDGE_CURVE('',#4486,#4486,#2362,.T.);
#5614=EDGE_CURVE('',#4487,#4488,#2363,.T.);
#5615=EDGE_CURVE('',#4488,#4489,#2998,.T.);
#5616=EDGE_CURVE('',#4489,#4489,#2364,.T.);
#5617=EDGE_CURVE('',#4488,#4487,#2365,.T.);
#5618=EDGE_CURVE('',#4490,#4491,#2366,.T.);
#5619=EDGE_CURVE('',#4490,#4492,#2367,.T.);
#5620=EDGE_CURVE('',#4493,#4492,#2999,.T.);
#5621=EDGE_CURVE('',#4493,#4494,#2368,.T.);
#5622=EDGE_CURVE('',#4495,#4494,#2369,.T.);
#5623=EDGE_CURVE('',#4495,#4496,#2370,.T.);
#5624=EDGE_CURVE('',#4497,#4496,#3000,.T.);
#5625=EDGE_CURVE('',#4497,#4491,#2371,.T.);
#5626=EDGE_CURVE('',#4498,#4499,#2372,.T.);
#5627=EDGE_CURVE('',#4498,#4490,#3001,.T.);
#5628=EDGE_CURVE('',#4491,#4499,#3002,.T.);
#5629=EDGE_CURVE('',#4496,#4500,#3003,.T.);
#5630=EDGE_CURVE('',#4501,#4500,#3004,.T.);
#5631=EDGE_CURVE('',#4501,#4497,#3005,.T.);
#5632=EDGE_CURVE('',#4494,#4502,#3006,.T.);
#5633=EDGE_CURVE('',#4503,#4502,#2373,.T.);
#5634=EDGE_CURVE('',#4503,#4495,#3007,.T.);
#5635=EDGE_CURVE('',#4492,#4504,#3008,.T.);
#5636=EDGE_CURVE('',#4505,#4504,#3009,.T.);
#5637=EDGE_CURVE('',#4505,#4493,#3010,.T.);
#5638=EDGE_CURVE('',#4504,#4498,#2374,.T.);
#5639=EDGE_CURVE('',#4499,#4501,#2375,.T.);
#5640=EDGE_CURVE('',#4500,#4503,#2376,.T.);
#5641=EDGE_CURVE('',#4502,#4505,#2377,.T.);
#5642=EDGE_CURVE('',#4506,#4506,#2378,.T.);
#5643=EDGE_CURVE('',#4506,#4485,#3011,.T.);
#5644=EDGE_CURVE('',#4481,#4480,#3012,.T.);
#5645=EDGE_CURVE('',#4487,#4486,#3013,.T.);
#7586=ORIENTED_EDGE('',*,*,#5606,.T.);
#7587=ORIENTED_EDGE('',*,*,#5607,.T.);
#7588=ORIENTED_EDGE('',*,*,#5608,.T.);
#7589=ORIENTED_EDGE('',*,*,#5609,.T.);
#7590=ORIENTED_EDGE('',*,*,#5608,.F.);
#7591=ORIENTED_EDGE('',*,*,#5610,.T.);
#7592=ORIENTED_EDGE('',*,*,#5611,.F.);
#7593=ORIENTED_EDGE('',*,*,#5612,.F.);
#7594=ORIENTED_EDGE('',*,*,#5613,.T.);
#7595=ORIENTED_EDGE('',*,*,#5609,.F.);
#7596=ORIENTED_EDGE('',*,*,#5614,.T.);
#7597=ORIENTED_EDGE('',*,*,#5615,.T.);
#7598=ORIENTED_EDGE('',*,*,#5616,.T.);
#7599=ORIENTED_EDGE('',*,*,#5615,.F.);
#7600=ORIENTED_EDGE('',*,*,#5617,.T.);
#7601=ORIENTED_EDGE('',*,*,#5616,.F.);
#7602=ORIENTED_EDGE('',*,*,#5618,.F.);
#7603=ORIENTED_EDGE('',*,*,#5619,.T.);
#7604=ORIENTED_EDGE('',*,*,#5620,.F.);
#7605=ORIENTED_EDGE('',*,*,#5621,.T.);
#7606=ORIENTED_EDGE('',*,*,#5622,.F.);
#7607=ORIENTED_EDGE('',*,*,#5623,.T.);
#7608=ORIENTED_EDGE('',*,*,#5624,.F.);
#7609=ORIENTED_EDGE('',*,*,#5625,.T.);
#7610=ORIENTED_EDGE('',*,*,#5626,.F.);
#7611=ORIENTED_EDGE('',*,*,#5627,.T.);
#7612=ORIENTED_EDGE('',*,*,#5618,.T.);
#7613=ORIENTED_EDGE('',*,*,#5628,.T.);
#7614=ORIENTED_EDGE('',*,*,#5624,.T.);
#7615=ORIENTED_EDGE('',*,*,#5629,.T.);
#7616=ORIENTED_EDGE('',*,*,#5630,.F.);
#7617=ORIENTED_EDGE('',*,*,#5631,.T.);
#7618=ORIENTED_EDGE('',*,*,#5622,.T.);
#7619=ORIENTED_EDGE('',*,*,#5632,.T.);
#7620=ORIENTED_EDGE('',*,*,#5633,.F.);
#7621=ORIENTED_EDGE('',*,*,#5634,.T.);
#7622=ORIENTED_EDGE('',*,*,#5620,.T.);
#7623=ORIENTED_EDGE('',*,*,#5635,.T.);
#7624=ORIENTED_EDGE('',*,*,#5636,.F.);
#7625=ORIENTED_EDGE('',*,*,#5637,.T.);
#7626=ORIENTED_EDGE('',*,*,#5636,.T.);
#7627=ORIENTED_EDGE('',*,*,#5638,.T.);
#7628=ORIENTED_EDGE('',*,*,#5626,.T.);
#7629=ORIENTED_EDGE('',*,*,#5639,.T.);
#7630=ORIENTED_EDGE('',*,*,#5630,.T.);
#7631=ORIENTED_EDGE('',*,*,#5640,.T.);
#7632=ORIENTED_EDGE('',*,*,#5633,.T.);
#7633=ORIENTED_EDGE('',*,*,#5641,.T.);
#7634=ORIENTED_EDGE('',*,*,#5642,.F.);
#7635=ORIENTED_EDGE('',*,*,#5643,.T.);
#7636=ORIENTED_EDGE('',*,*,#5612,.T.);
#7637=ORIENTED_EDGE('',*,*,#5611,.T.);
#7638=ORIENTED_EDGE('',*,*,#5643,.F.);
#7639=ORIENTED_EDGE('',*,*,#5642,.T.);
#7640=ORIENTED_EDGE('',*,*,#5607,.F.);
#7641=ORIENTED_EDGE('',*,*,#5644,.T.);
#7642=ORIENTED_EDGE('',*,*,#5606,.F.);
#7643=ORIENTED_EDGE('',*,*,#5644,.F.);
#7644=ORIENTED_EDGE('',*,*,#5610,.F.);
#7645=ORIENTED_EDGE('',*,*,#5614,.F.);
#7646=ORIENTED_EDGE('',*,*,#5645,.T.);
#7647=ORIENTED_EDGE('',*,*,#5613,.F.);
#7648=ORIENTED_EDGE('',*,*,#5645,.F.);
#7649=ORIENTED_EDGE('',*,*,#5617,.F.);
#7650=ORIENTED_EDGE('',*,*,#5638,.F.);
#7651=ORIENTED_EDGE('',*,*,#5635,.F.);
#7652=ORIENTED_EDGE('',*,*,#5619,.F.);
#7653=ORIENTED_EDGE('',*,*,#5627,.F.);
#7654=ORIENTED_EDGE('',*,*,#5641,.F.);
#7655=ORIENTED_EDGE('',*,*,#5632,.F.);
#7656=ORIENTED_EDGE('',*,*,#5621,.F.);
#7657=ORIENTED_EDGE('',*,*,#5637,.F.);
#7658=ORIENTED_EDGE('',*,*,#5640,.F.);
#7659=ORIENTED_EDGE('',*,*,#5629,.F.);
#7660=ORIENTED_EDGE('',*,*,#5623,.F.);
#7661=ORIENTED_EDGE('',*,*,#5634,.F.);
#7662=ORIENTED_EDGE('',*,*,#5639,.F.);
#7663=ORIENTED_EDGE('',*,*,#5628,.F.);
#7664=ORIENTED_EDGE('',*,*,#5625,.F.);
#7665=ORIENTED_EDGE('',*,*,#5631,.F.);
#9280=CYLINDRICAL_SURFACE('',#10629,5.);
#9281=CYLINDRICAL_SURFACE('',#10635,15.);
#9282=CYLINDRICAL_SURFACE('',#10646,12.5);
#9283=CYLINDRICAL_SURFACE('',#10649,12.5);
#9284=CYLINDRICAL_SURFACE('',#10657,2.8);
#9285=CYLINDRICAL_SURFACE('',#10662,1.);
#9286=CYLINDRICAL_SURFACE('',#10663,1.);
#9287=CYLINDRICAL_SURFACE('',#10664,1.);
#9288=CYLINDRICAL_SURFACE('',#10665,1.);
#9604=ADVANCED_FACE('',(#1238),#887,.T.);
#9605=ADVANCED_FACE('',(#1239,#493),#9280,.T.);
#9606=ADVANCED_FACE('',(#1240,#494),#888,.T.);
#9607=ADVANCED_FACE('',(#1241),#9281,.T.);
#9608=ADVANCED_FACE('',(#1242,#495),#889,.T.);
#9609=ADVANCED_FACE('',(#1243),#9282,.T.);
#9610=ADVANCED_FACE('',(#1244),#890,.F.);
#9611=ADVANCED_FACE('',(#1245),#9283,.T.);
#9612=ADVANCED_FACE('',(#1246),#891,.F.);
#9613=ADVANCED_FACE('',(#1247),#892,.T.);
#9614=ADVANCED_FACE('',(#1248),#9284,.F.);
#9615=ADVANCED_FACE('',(#1249),#893,.T.);
#9616=ADVANCED_FACE('',(#1250),#353,.T.);
#9617=ADVANCED_FACE('',(#1251),#354,.T.);
#9618=ADVANCED_FACE('',(#1252),#9285,.T.);
#9619=ADVANCED_FACE('',(#1253),#9286,.T.);
#9620=ADVANCED_FACE('',(#1254),#9287,.T.);
#9621=ADVANCED_FACE('',(#1255),#9288,.T.);
#9946=CLOSED_SHELL('',(#9604,#9605,#9606,#9607,#9608,#9609,#9610,#9611,
#9612,#9613,#9614,#9615,#9616,#9617,#9618,#9619,#9620,#9621));
#10626=AXIS2_PLACEMENT_3D('',#17992,#12348,#12349);
#10627=AXIS2_PLACEMENT_3D('',#17993,#12350,#12351);
#10628=AXIS2_PLACEMENT_3D('',#17995,#12352,#12353);
#10629=AXIS2_PLACEMENT_3D('',#17996,#12354,#12355);
#10630=AXIS2_PLACEMENT_3D('',#17999,#12356,#12357);
#10631=AXIS2_PLACEMENT_3D('',#18002,#12359,#12360);
#10632=AXIS2_PLACEMENT_3D('',#18003,#12361,#12362);
#10633=AXIS2_PLACEMENT_3D('',#18042,#12363,#12364);
#10634=AXIS2_PLACEMENT_3D('',#18044,#12365,#12366);
#10635=AXIS2_PLACEMENT_3D('',#18045,#12367,#12368);
#10636=AXIS2_PLACEMENT_3D('',#18048,#12369,#12370);
#10637=AXIS2_PLACEMENT_3D('',#18051,#12372,#12373);
#10638=AXIS2_PLACEMENT_3D('',#18052,#12374,#12375);
#10639=AXIS2_PLACEMENT_3D('',#18053,#12376,#12377);
#10640=AXIS2_PLACEMENT_3D('',#18056,#12378,#12379);
#10641=AXIS2_PLACEMENT_3D('',#18058,#12380,#12381);
#10642=AXIS2_PLACEMENT_3D('',#18062,#12383,#12384);
#10643=AXIS2_PLACEMENT_3D('',#18064,#12385,#12386);
#10644=AXIS2_PLACEMENT_3D('',#18066,#12387,#12388);
#10645=AXIS2_PLACEMENT_3D('',#18069,#12390,#12391);
#10646=AXIS2_PLACEMENT_3D('',#18070,#12392,#12393);
#10647=AXIS2_PLACEMENT_3D('',#18073,#12394,#12395);
#10648=AXIS2_PLACEMENT_3D('',#18076,#12398,#12399);
#10649=AXIS2_PLACEMENT_3D('',#18082,#12403,#12404);
#10650=AXIS2_PLACEMENT_3D('',#18086,#12406,#12407);
#10651=AXIS2_PLACEMENT_3D('',#18088,#12409,#12410);
#10652=AXIS2_PLACEMENT_3D('',#18094,#12414,#12415);
#10653=AXIS2_PLACEMENT_3D('',#18095,#12416,#12417);
#10654=AXIS2_PLACEMENT_3D('',#18096,#12418,#12419);
#10655=AXIS2_PLACEMENT_3D('',#18097,#12420,#12421);
#10656=AXIS2_PLACEMENT_3D('',#18098,#12422,#12423);
#10657=AXIS2_PLACEMENT_3D('',#18099,#12424,#12425);
#10658=AXIS2_PLACEMENT_3D('',#18101,#12426,#12427);
#10659=AXIS2_PLACEMENT_3D('',#18103,#12429,#12430);
#10660=AXIS2_PLACEMENT_3D('',#18104,#12431,#12432);
#10661=AXIS2_PLACEMENT_3D('',#18106,#12434,#12435);
#10662=AXIS2_PLACEMENT_3D('',#18108,#12437,#12438);
#10663=AXIS2_PLACEMENT_3D('',#18109,#12439,#12440);
#10664=AXIS2_PLACEMENT_3D('',#18110,#12441,#12442);
#10665=AXIS2_PLACEMENT_3D('',#18111,#12443,#12444);
#12348=DIRECTION('axis',(0.,0.,1.));
#12349=DIRECTION('refdir',(1.,0.,0.));
#12350=DIRECTION('center_axis',(0.,-1.,0.));
#12351=DIRECTION('ref_axis',(0.,0.,-1.));
#12352=DIRECTION('center_axis',(0.,-1.,0.));
#12353=DIRECTION('ref_axis',(0.,0.,-1.));
#12354=DIRECTION('center_axis',(0.,-1.,0.));
#12355=DIRECTION('ref_axis',(0.,0.,-1.));
#12356=DIRECTION('center_axis',(0.,1.,0.));
#12357=DIRECTION('ref_axis',(0.,0.,-1.));
#12358=DIRECTION('',(0.,1.,0.));
#12359=DIRECTION('center_axis',(0.,-1.,0.));
#12360=DIRECTION('ref_axis',(0.,0.,-1.));
#12361=DIRECTION('center_axis',(0.,1.,0.));
#12362=DIRECTION('ref_axis',(0.,0.,-1.));
#12363=DIRECTION('center_axis',(0.,-1.,0.));
#12364=DIRECTION('ref_axis',(0.,0.,-1.));
#12365=DIRECTION('center_axis',(0.,-1.,0.));
#12366=DIRECTION('ref_axis',(0.,0.,-1.));
#12367=DIRECTION('center_axis',(0.,-1.,0.));
#12368=DIRECTION('ref_axis',(0.,0.,-1.));
#12369=DIRECTION('center_axis',(0.,1.,0.));
#12370=DIRECTION('ref_axis',(0.,0.,-1.));
#12371=DIRECTION('',(0.,1.,0.));
#12372=DIRECTION('center_axis',(0.,-1.,0.));
#12373=DIRECTION('ref_axis',(0.,0.,-1.));
#12374=DIRECTION('center_axis',(0.,1.,0.));
#12375=DIRECTION('ref_axis',(0.,0.,-1.));
#12376=DIRECTION('center_axis',(0.,1.,0.));
#12377=DIRECTION('ref_axis',(0.,0.,1.));
#12378=DIRECTION('center_axis',(0.,1.,0.));
#12379=DIRECTION('ref_axis',(0.,0.,1.));
#12380=DIRECTION('center_axis',(0.,-1.,0.));
#12381=DIRECTION('ref_axis',(0.,0.,1.));
#12382=DIRECTION('',(-1.,0.,0.));
#12383=DIRECTION('center_axis',(0.,-1.,0.));
#12384=DIRECTION('ref_axis',(0.,0.,1.));
#12385=DIRECTION('center_axis',(0.,1.,0.));
#12386=DIRECTION('ref_axis',(0.,0.,1.));
#12387=DIRECTION('center_axis',(0.,-1.,0.));
#12388=DIRECTION('ref_axis',(1.73472347597681E-15,0.,1.));
#12389=DIRECTION('',(1.,0.,0.));
#12390=DIRECTION('center_axis',(0.,-1.,0.));
#12391=DIRECTION('ref_axis',(0.,0.,1.));
#12392=DIRECTION('center_axis',(0.,-1.,0.));
#12393=DIRECTION('ref_axis',(0.,0.,-1.));
#12394=DIRECTION('center_axis',(0.,1.,0.));
#12395=DIRECTION('ref_axis',(0.,0.,1.));
#12396=DIRECTION('',(0.,-1.,0.));
#12397=DIRECTION('',(0.,1.,0.));
#12398=DIRECTION('center_axis',(0.,0.,-1.));
#12399=DIRECTION('ref_axis',(-1.,0.,0.));
#12400=DIRECTION('',(0.,1.,0.));
#12401=DIRECTION('',(1.,0.,0.));
#12402=DIRECTION('',(0.,-1.,0.));
#12403=DIRECTION('center_axis',(0.,-1.,0.));
#12404=DIRECTION('ref_axis',(0.,0.,-1.));
#12405=DIRECTION('',(0.,1.,0.));
#12406=DIRECTION('center_axis',(0.,1.,0.));
#12407=DIRECTION('ref_axis',(0.,0.,1.));
#12408=DIRECTION('',(0.,-1.,0.));
#12409=DIRECTION('center_axis',(0.,0.,1.));
#12410=DIRECTION('ref_axis',(1.,0.,0.));
#12411=DIRECTION('',(0.,1.,0.));
#12412=DIRECTION('',(-1.,0.,0.));
#12413=DIRECTION('',(0.,-1.,0.));
#12414=DIRECTION('center_axis',(0.,1.,0.));
#12415=DIRECTION('ref_axis',(0.,0.,1.));
#12416=DIRECTION('center_axis',(0.,1.,0.));
#12417=DIRECTION('ref_axis',(0.,0.,1.));
#12418=DIRECTION('center_axis',(0.,1.,0.));
#12419=DIRECTION('ref_axis',(0.,0.,1.));
#12420=DIRECTION('center_axis',(0.,1.,0.));
#12421=DIRECTION('ref_axis',(0.,0.,1.));
#12422=DIRECTION('center_axis',(0.,1.,0.));
#12423=DIRECTION('ref_axis',(0.,0.,1.));
#12424=DIRECTION('center_axis',(1.,0.,0.));
#12425=DIRECTION('ref_axis',(0.,0.,-1.));
#12426=DIRECTION('center_axis',(1.,0.,0.));
#12427=DIRECTION('ref_axis',(0.,0.,-1.));
#12428=DIRECTION('',(1.,0.,0.));
#12429=DIRECTION('center_axis',(1.,0.,0.));
#12430=DIRECTION('ref_axis',(0.,0.,-1.));
#12431=DIRECTION('center_axis',(0.,1.,0.));
#12432=DIRECTION('ref_axis',(0.,0.,1.));
#12433=DIRECTION('',(8.6595605623549E-17,-0.70710678118655,0.707106781186545));
#12434=DIRECTION('center_axis',(0.,1.,0.));
#12435=DIRECTION('ref_axis',(0.,0.,1.));
#12436=DIRECTION('',(8.65956056235492E-17,-0.707106781186549,0.707106781186546));
#12437=DIRECTION('center_axis',(0.,-1.,0.));
#12438=DIRECTION('ref_axis',(0.,0.,-1.));
#12439=DIRECTION('center_axis',(0.,-1.,0.));
#12440=DIRECTION('ref_axis',(0.,0.,-1.));
#12441=DIRECTION('center_axis',(0.,-1.,0.));
#12442=DIRECTION('ref_axis',(0.,0.,-1.));
#12443=DIRECTION('center_axis',(0.,-1.,0.));
#12444=DIRECTION('ref_axis',(0.,0.,-1.));
#17992=CARTESIAN_POINT('',(0.,0.,0.));
#17993=CARTESIAN_POINT('Origin',(0.,0.,0.));
#17994=CARTESIAN_POINT('',(0.,0.,-4.50000000000001));
#17995=CARTESIAN_POINT('Origin',(0.,0.,0.));
#17996=CARTESIAN_POINT('Origin',(0.,0.,0.));
#17997=CARTESIAN_POINT('',(0.,0.499999999999993,-5.));
#17998=CARTESIAN_POINT('',(-6.12323399573677E-16,0.499999999999993,5.));
#17999=CARTESIAN_POINT('Origin',(0.,0.499999999999993,0.));
#18000=CARTESIAN_POINT('',(-6.12323399573677E-16,12.9,5.));
#18001=CARTESIAN_POINT('',(-6.12323399573677E-16,0.,5.));
#18002=CARTESIAN_POINT('Origin',(0.,12.9,0.));
#18003=CARTESIAN_POINT('Origin',(0.,0.499999999999993,0.));
#18004=CARTESIAN_POINT('',(4.1424630354416,5.9,-2.8));
#18005=CARTESIAN_POINT('',(4.1424630354416,5.9,2.8));
#18006=CARTESIAN_POINT('Ctrl Pts',(4.1424630354416,5.9,-2.8));
#18007=CARTESIAN_POINT('Ctrl Pts',(4.1424630354416,6.2618023460428,-2.8));
#18008=CARTESIAN_POINT('Ctrl Pts',(4.19489580586978,6.63981714967516,-2.72600153733785));
#18009=CARTESIAN_POINT('Ctrl Pts',(4.36844276781151,7.3260008314647,-2.43822468472126));
#18010=CARTESIAN_POINT('Ctrl Pts',(4.48577042903711,7.63518970310634,-2.22460827153833));
#18011=CARTESIAN_POINT('Ctrl Pts',(4.69633401466985,8.1234771250952,-1.73632084954946));
#18012=CARTESIAN_POINT('Ctrl Pts',(4.80503654476778,8.33790022851277,-1.42678909437522));
#18013=CARTESIAN_POINT('Ctrl Pts',(4.9576268468014,8.62636123824948,-0.738944846559111));
#18014=CARTESIAN_POINT('Ctrl Pts',(5.,8.7,-0.360129947555138));
#18015=CARTESIAN_POINT('Ctrl Pts',(5.,8.7,0.360129947555139));
#18016=CARTESIAN_POINT('Ctrl Pts',(4.9576268468014,8.62636123824948,0.738944846559112));
#18017=CARTESIAN_POINT('Ctrl Pts',(4.80503654476778,8.33790022851277,1.42678909437522));
#18018=CARTESIAN_POINT('Ctrl Pts',(4.69633401466985,8.1234771250952,1.73632084954946));
#18019=CARTESIAN_POINT('Ctrl Pts',(4.48577042903712,7.63518970310634,2.22460827153833));
#18020=CARTESIAN_POINT('Ctrl Pts',(4.36844276781151,7.3260008314647,2.43822468472126));
#18021=CARTESIAN_POINT('Ctrl Pts',(4.19489580586978,6.63981714967516,2.72600153733785));
#18022=CARTESIAN_POINT('Ctrl Pts',(4.1424630354416,6.2618023460428,2.8));
#18023=CARTESIAN_POINT('Ctrl Pts',(4.1424630354416,5.9,2.8));
#18024=CARTESIAN_POINT('Ctrl Pts',(4.1424630354416,5.9,2.8));
#18025=CARTESIAN_POINT('Ctrl Pts',(4.1424630354416,5.5381976539572,2.8));
#18026=CARTESIAN_POINT('Ctrl Pts',(4.19489580586978,5.16018285032483,2.72600153733785));
#18027=CARTESIAN_POINT('Ctrl Pts',(4.36844276781151,4.4739991685353,2.43822468472126));
#18028=CARTESIAN_POINT('Ctrl Pts',(4.48577042903712,4.16481029689366,2.22460827153833));
#18029=CARTESIAN_POINT('Ctrl Pts',(4.69633401466985,3.67652287490479,1.73632084954946));
#18030=CARTESIAN_POINT('Ctrl Pts',(4.80503654476778,3.46209977148723,1.42678909437522));
#18031=CARTESIAN_POINT('Ctrl Pts',(4.9576268468014,3.17363876175052,0.73894484655911));
#18032=CARTESIAN_POINT('Ctrl Pts',(5.,3.1,0.360129947555138));
#18033=CARTESIAN_POINT('Ctrl Pts',(5.,3.1,-0.360129947555139));
#18034=CARTESIAN_POINT('Ctrl Pts',(4.9576268468014,3.17363876175052,-0.738944846559111));
#18035=CARTESIAN_POINT('Ctrl Pts',(4.80503654476778,3.46209977148723,-1.42678909437522));
#18036=CARTESIAN_POINT('Ctrl Pts',(4.69633401466985,3.67652287490479,-1.73632084954946));
#18037=CARTESIAN_POINT('Ctrl Pts',(4.48577042903711,4.16481029689366,-2.22460827153833));
#18038=CARTESIAN_POINT('Ctrl Pts',(4.36844276781151,4.4739991685353,-2.43822468472126));
#18039=CARTESIAN_POINT('Ctrl Pts',(4.19489580586978,5.16018285032483,-2.72600153733785));
#18040=CARTESIAN_POINT('Ctrl Pts',(4.1424630354416,5.5381976539572,-2.8));
#18041=CARTESIAN_POINT('Ctrl Pts',(4.1424630354416,5.9,-2.8));
#18042=CARTESIAN_POINT('Origin',(5.,12.9,0.));
#18043=CARTESIAN_POINT('',(0.,12.9,-14.5));
#18044=CARTESIAN_POINT('Origin',(0.,12.9,0.));
#18045=CARTESIAN_POINT('Origin',(0.,0.,0.));
#18046=CARTESIAN_POINT('',(0.,13.4,-15.));
#18047=CARTESIAN_POINT('',(-1.83697019872103E-15,13.4,15.));
#18048=CARTESIAN_POINT('Origin',(0.,13.4,0.));
#18049=CARTESIAN_POINT('',(-1.83697019872103E-15,15.9,15.));
#18050=CARTESIAN_POINT('',(-1.83697019872103E-15,0.,15.));
#18051=CARTESIAN_POINT('Origin',(0.,15.9,0.));
#18052=CARTESIAN_POINT('Origin',(0.,13.4,0.));
#18053=CARTESIAN_POINT('Origin',(15.,15.9,0.));
#18054=CARTESIAN_POINT('',(-12.2997907907885,15.9,-2.22826086956522));
#18055=CARTESIAN_POINT('',(-12.2997907907885,15.9,2.22826086956522));
#18056=CARTESIAN_POINT('Origin',(0.,15.9,0.));
#18057=CARTESIAN_POINT('',(-11.3158075275254,15.9,-3.05));
#18058=CARTESIAN_POINT('Origin',(-11.3158075275254,15.9,-2.05));
#18059=CARTESIAN_POINT('',(11.3158075275254,15.9,-3.05));
#18060=CARTESIAN_POINT('',(-12.1221903961289,15.9,-3.05));
#18061=CARTESIAN_POINT('',(12.2997907907885,15.9,-2.22826086956522));
#18062=CARTESIAN_POINT('Origin',(11.3158075275254,15.9,-2.05));
#18063=CARTESIAN_POINT('',(12.2997907907885,15.9,2.22826086956522));
#18064=CARTESIAN_POINT('Origin',(0.,15.9,0.));
#18065=CARTESIAN_POINT('',(11.3158075275254,15.9,3.05));
#18066=CARTESIAN_POINT('Origin',(11.3158075275254,15.9,2.05));
#18067=CARTESIAN_POINT('',(-11.3158075275254,15.9,3.05));
#18068=CARTESIAN_POINT('',(-12.1221903961289,15.9,3.05));
#18069=CARTESIAN_POINT('Origin',(-11.3158075275254,15.9,2.05));
#18070=CARTESIAN_POINT('Origin',(0.,20.9,0.));
#18071=CARTESIAN_POINT('',(-12.2997907907885,20.9,-2.22826086956522));
#18072=CARTESIAN_POINT('',(-12.2997907907885,20.9,2.22826086956522));
#18073=CARTESIAN_POINT('Origin',(0.,20.9,0.));
#18074=CARTESIAN_POINT('',(-12.2997907907885,20.9,-2.22826086956522));
#18075=CARTESIAN_POINT('',(-12.2997907907885,20.9,2.22826086956522));
#18076=CARTESIAN_POINT('Origin',(-12.1221903961289,20.9,3.05));
#18077=CARTESIAN_POINT('',(11.3158075275254,20.9,3.05));
#18078=CARTESIAN_POINT('',(11.3158075275254,20.9,3.05));
#18079=CARTESIAN_POINT('',(-11.3158075275254,20.9,3.05));
#18080=CARTESIAN_POINT('',(-12.1221903961289,20.9,3.05));
#18081=CARTESIAN_POINT('',(-11.3158075275254,20.9,3.05));
#18082=CARTESIAN_POINT('Origin',(0.,20.9,0.));
#18083=CARTESIAN_POINT('',(12.2997907907885,20.9,-2.22826086956522));
#18084=CARTESIAN_POINT('',(12.2997907907885,20.9,-2.22826086956522));
#18085=CARTESIAN_POINT('',(12.2997907907885,20.9,2.22826086956522));
#18086=CARTESIAN_POINT('Origin',(0.,20.9,0.));
#18087=CARTESIAN_POINT('',(12.2997907907885,20.9,2.22826086956522));
#18088=CARTESIAN_POINT('Origin',(-12.1221903961289,20.9,-3.05));
#18089=CARTESIAN_POINT('',(-11.3158075275254,20.9,-3.05));
#18090=CARTESIAN_POINT('',(-11.3158075275254,20.9,-3.05));
#18091=CARTESIAN_POINT('',(11.3158075275254,20.9,-3.05));
#18092=CARTESIAN_POINT('',(-12.1221903961289,20.9,-3.05));
#18093=CARTESIAN_POINT('',(11.3158075275254,20.9,-3.05));
#18094=CARTESIAN_POINT('Origin',(0.,20.9,0.));
#18095=CARTESIAN_POINT('Origin',(-11.3158075275254,20.9,-2.05));
#18096=CARTESIAN_POINT('Origin',(-11.3158075275254,20.9,2.05));
#18097=CARTESIAN_POINT('Origin',(11.3158075275254,20.9,2.05));
#18098=CARTESIAN_POINT('Origin',(11.3158075275254,20.9,-2.05));
#18099=CARTESIAN_POINT('Origin',(-2.5,5.9,0.));
#18100=CARTESIAN_POINT('',(-2.5,5.9,2.8));
#18101=CARTESIAN_POINT('Origin',(-2.5,5.9,0.));
#18102=CARTESIAN_POINT('',(-2.5,5.9,2.8));
#18103=CARTESIAN_POINT('Origin',(-2.5,5.9,0.));
#18104=CARTESIAN_POINT('Origin',(0.,0.,0.));
#18105=CARTESIAN_POINT('',(-5.5109105961631E-16,0.,-4.50000000000001));
#18106=CARTESIAN_POINT('Origin',(0.,12.9,0.));
#18107=CARTESIAN_POINT('',(-1.77573785876366E-15,12.9,-14.5));
#18108=CARTESIAN_POINT('Origin',(-11.3158075275254,20.9,-2.05));
#18109=CARTESIAN_POINT('Origin',(11.3158075275254,20.9,-2.05));
#18110=CARTESIAN_POINT('Origin',(11.3158075275254,20.9,2.05));
#18111=CARTESIAN_POINT('Origin',(-11.3158075275254,20.9,2.05));
#32959=UNCERTAINTY_MEASURE_WITH_UNIT(LENGTH_MEASURE(0.01),#33017,
'DISTANCE_ACCURACY_VALUE',
'Maximum model space distance between geometric entities at asserted c
onnectivities');
#32984=UNCERTAINTY_MEASURE_WITH_UNIT(LENGTH_MEASURE(0.01),#33017,
'DISTANCE_ACCURACY_VALUE',
'Maximum model space distance between geometric entities at asserted c
onnectivities');
#32991=(
GEOMETRIC_REPRESENTATION_CONTEXT(3)
GLOBAL_UNCERTAINTY_ASSIGNED_CONTEXT((#32959))
GLOBAL_UNIT_ASSIGNED_CONTEXT((#33017,#33019,#33020))
REPRESENTATION_CONTEXT('','3D')
);
#33016=(
GEOMETRIC_REPRESENTATION_CONTEXT(3)
GLOBAL_UNCERTAINTY_ASSIGNED_CONTEXT((#32984))
GLOBAL_UNIT_ASSIGNED_CONTEXT((#33017,#33019,#33020))
REPRESENTATION_CONTEXT('','3D')
);
#33017=(
LENGTH_UNIT()
NAMED_UNIT(*)
SI_UNIT(.MILLI.,.METRE.)
);
#33019=(
NAMED_UNIT(*)
PLANE_ANGLE_UNIT()
SI_UNIT($,.RADIAN.)
);
#33020=(
NAMED_UNIT(*)
SI_UNIT($,.STERADIAN.)
SOLID_ANGLE_UNIT()
);
#33027=SHAPE_DEFINITION_REPRESENTATION(#33058,#33130);
#33058=PRODUCT_DEFINITION_SHAPE('',$,#33162);
#33130=SHAPE_REPRESENTATION('',(#10626),#32991);
#33155=PRODUCT_DEFINITION_CONTEXT('part definition',#33250,'design');
#33162=PRODUCT_DEFINITION('P_Torque Wrench_Knob_PRT-RH-1004-04_M_Rev02',
'PRT-RH-1004-04',#33193,#33155);
#33193=PRODUCT_DEFINITION_FORMATION('',$,#33258);
#33250=APPLICATION_CONTEXT(
'Core Data for Automotive Mechanical Design Process');
#33251=PRODUCT_CONTEXT('part definition',#33250,'mechanical');
#33258=PRODUCT('P_Torque Wrench_Knob_PRT-RH-1004-04_M_Rev02',
'PRT-RH-1004-04',$,(#33251));
#33284=PRESENTATION_STYLE_ASSIGNMENT((#33291));
#33291=SURFACE_STYLE_USAGE(.BOTH.,#33298);
#33298=SURFACE_SIDE_STYLE('',(#33305));
#33305=SURFACE_STYLE_FILL_AREA(#33312);
#33312=FILL_AREA_STYLE('Opaque(186,91,6)',(#33319));
#33319=FILL_AREA_STYLE_COLOUR('Opaque(186,91,6)',#33326);
#33326=COLOUR_RGB('Opaque(186,91,6)', 0.09019608, 0.27058824, 0.51372549);
ENDSEC;
END-ISO-10303-21;
